ISO-10303-21;
HEADER;
/* Generated by software containing ST-Developer
 * from STEP Tools, Inc. (www.steptools.com) 
 */

FILE_DESCRIPTION(
/* description */ ('STEP AP214'),
/* implementation_level */ '2;1');

FILE_NAME(
/* name */ 'Hex Nut M8.step',
/* time_stamp */ '2026-11-14T06:10:26-08:00',
/* author */ (''),
/* organization */ (''),
/* preprocessor_version */ 'ST-DEVELOPER v20.2',
/* originating_system */ 'Autodesk Translation Framework v15.17.0.0',
/* authorisation */ '');

FILE_SCHEMA (('AUTOMOTIVE_DESIGN { 1 0 10303 214 3 1 1 }'));
ENDSEC;

DATA;
#10=MECHANICAL_DESIGN_GEOMETRIC_PRESENTATION_REPRESENTATION('',(#167),#10413);
#90=(
BOUNDED_CURVE()
B_SPLINE_CURVE(2,(#9232,#9233,#9234),.UNSPECIFIED.,.F.,.F.)
B_SPLINE_CURVE_WITH_KNOTS((3,3),(-2.73681737299457,-1.98462831214807),
 .UNSPECIFIED.)
CURVE()
GEOMETRIC_REPRESENTATION_ITEM()
RATIONAL_B_SPLINE_CURVE((1.85571966561192,1.99926008128974,1.99926008128974))
REPRESENTATION_ITEM('')
);
#91=(
BOUNDED_CURVE()
B_SPLINE_CURVE(2,(#9235,#9236,#9237),.UNSPECIFIED.,.F.,.F.)
B_SPLINE_CURVE_WITH_KNOTS((3,3),(1.98462831214807,2.73681737299457),
 .UNSPECIFIED.)
CURVE()
GEOMETRIC_REPRESENTATION_ITEM()
RATIONAL_B_SPLINE_CURVE((1.99926008128974,1.99926008128974,1.85571966561192))
REPRESENTATION_ITEM('')
);
#92=(
BOUNDED_CURVE()
B_SPLINE_CURVE(2,(#9243,#9244,#9245),.UNSPECIFIED.,.F.,.F.)
B_SPLINE_CURVE_WITH_KNOTS((3,3),(1.98462831214807,2.73681737299457),
 .UNSPECIFIED.)
CURVE()
GEOMETRIC_REPRESENTATION_ITEM()
RATIONAL_B_SPLINE_CURVE((1.99926008128974,1.99926008128974,1.85571966561192))
REPRESENTATION_ITEM('')
);
#93=(
BOUNDED_CURVE()
B_SPLINE_CURVE(2,(#9246,#9247,#9248),.UNSPECIFIED.,.F.,.F.)
B_SPLINE_CURVE_WITH_KNOTS((3,3),(-2.73681737299457,-1.98462831214807),
 .UNSPECIFIED.)
CURVE()
GEOMETRIC_REPRESENTATION_ITEM()
RATIONAL_B_SPLINE_CURVE((1.85571966561192,1.99926008128974,1.99926008128974))
REPRESENTATION_ITEM('')
);
#94=(
BOUNDED_CURVE()
B_SPLINE_CURVE(2,(#9252,#9253,#9254),.UNSPECIFIED.,.F.,.F.)
B_SPLINE_CURVE_WITH_KNOTS((3,3),(-1.98462831214807,-1.23243925130156),
 .UNSPECIFIED.)
CURVE()
GEOMETRIC_REPRESENTATION_ITEM()
RATIONAL_B_SPLINE_CURVE((1.99926008128974,1.99926008128975,1.85571966561192))
REPRESENTATION_ITEM('')
);
#95=(
BOUNDED_CURVE()
B_SPLINE_CURVE(2,(#9257,#9258,#9259),.UNSPECIFIED.,.F.,.F.)
B_SPLINE_CURVE_WITH_KNOTS((3,3),(1.98462831214807,2.73681737299457),
 .UNSPECIFIED.)
CURVE()
GEOMETRIC_REPRESENTATION_ITEM()
RATIONAL_B_SPLINE_CURVE((1.99926008128974,1.99926008128974,1.85571966561192))
REPRESENTATION_ITEM('')
);
#96=(
BOUNDED_CURVE()
B_SPLINE_CURVE(2,(#9264,#9265,#9266),.UNSPECIFIED.,.F.,.F.)
B_SPLINE_CURVE_WITH_KNOTS((3,3),(-2.73681737299457,-1.98462831214807),
 .UNSPECIFIED.)
CURVE()
GEOMETRIC_REPRESENTATION_ITEM()
RATIONAL_B_SPLINE_CURVE((1.85571966561192,1.99926008128974,1.99926008128974))
REPRESENTATION_ITEM('')
);
#97=(
BOUNDED_CURVE()
B_SPLINE_CURVE(2,(#9267,#9268,#9269),.UNSPECIFIED.,.F.,.F.)
B_SPLINE_CURVE_WITH_KNOTS((3,3),(1.23243925130156,1.98462831214807),
 .UNSPECIFIED.)
CURVE()
GEOMETRIC_REPRESENTATION_ITEM()
RATIONAL_B_SPLINE_CURVE((1.85571966561192,1.99926008128974,1.99926008128974))
REPRESENTATION_ITEM('')
);
#98=(
BOUNDED_CURVE()
B_SPLINE_CURVE(2,(#9275,#9276,#9277),.UNSPECIFIED.,.F.,.F.)
B_SPLINE_CURVE_WITH_KNOTS((3,3),(-2.73681737299457,-1.98462831214806),
 .UNSPECIFIED.)
CURVE()
GEOMETRIC_REPRESENTATION_ITEM()
RATIONAL_B_SPLINE_CURVE((1.85571966561192,1.99926008128974,1.99926008128974))
REPRESENTATION_ITEM('')
);
#99=(
BOUNDED_CURVE()
B_SPLINE_CURVE(2,(#9278,#9279,#9280),.UNSPECIFIED.,.F.,.F.)
B_SPLINE_CURVE_WITH_KNOTS((3,3),(-1.98462831214806,-1.23243925130156),
 .UNSPECIFIED.)
CURVE()
GEOMETRIC_REPRESENTATION_ITEM()
RATIONAL_B_SPLINE_CURVE((1.99926008128974,1.99926008128974,1.85571966561192))
REPRESENTATION_ITEM('')
);
#100=(
BOUNDED_CURVE()
B_SPLINE_CURVE(2,(#9282,#9283,#9284),.UNSPECIFIED.,.F.,.F.)
B_SPLINE_CURVE_WITH_KNOTS((3,3),(1.98462831214807,2.73681737299457),
 .UNSPECIFIED.)
CURVE()
GEOMETRIC_REPRESENTATION_ITEM()
RATIONAL_B_SPLINE_CURVE((1.99926008128974,1.99926008128974,1.85571966561192))
REPRESENTATION_ITEM('')
);
#101=(
BOUNDED_CURVE()
B_SPLINE_CURVE(2,(#9285,#9286,#9287),.UNSPECIFIED.,.F.,.F.)
B_SPLINE_CURVE_WITH_KNOTS((3,3),(1.23243925130156,1.98462831214807),
 .UNSPECIFIED.)
CURVE()
GEOMETRIC_REPRESENTATION_ITEM()
RATIONAL_B_SPLINE_CURVE((1.85571966561192,1.99926008128974,1.99926008128974))
REPRESENTATION_ITEM('')
);
#102=(
BOUNDED_CURVE()
B_SPLINE_CURVE(2,(#9293,#9294,#9295),.UNSPECIFIED.,.F.,.F.)
B_SPLINE_CURVE_WITH_KNOTS((3,3),(-2.73681737299457,-1.98462831214807),
 .UNSPECIFIED.)
CURVE()
GEOMETRIC_REPRESENTATION_ITEM()
RATIONAL_B_SPLINE_CURVE((1.85571966561192,1.99926008128974,1.99926008128974))
REPRESENTATION_ITEM('')
);
#103=(
BOUNDED_CURVE()
B_SPLINE_CURVE(2,(#9296,#9297,#9298),.UNSPECIFIED.,.F.,.F.)
B_SPLINE_CURVE_WITH_KNOTS((3,3),(-1.98462831214807,-1.23243925130157),
 .UNSPECIFIED.)
CURVE()
GEOMETRIC_REPRESENTATION_ITEM()
RATIONAL_B_SPLINE_CURVE((1.99926008128974,1.99926008128974,1.85571966561192))
REPRESENTATION_ITEM('')
);
#104=(
BOUNDED_CURVE()
B_SPLINE_CURVE(2,(#9300,#9301,#9302),.UNSPECIFIED.,.F.,.F.)
B_SPLINE_CURVE_WITH_KNOTS((3,3),(1.98462831214807,2.73681737299457),
 .UNSPECIFIED.)
CURVE()
GEOMETRIC_REPRESENTATION_ITEM()
RATIONAL_B_SPLINE_CURVE((1.99926008128974,1.99926008128974,1.85571966561192))
REPRESENTATION_ITEM('')
);
#105=(
BOUNDED_CURVE()
B_SPLINE_CURVE(2,(#9303,#9304,#9305),.UNSPECIFIED.,.F.,.F.)
B_SPLINE_CURVE_WITH_KNOTS((3,3),(1.23243925130156,1.98462831214807),
 .UNSPECIFIED.)
CURVE()
GEOMETRIC_REPRESENTATION_ITEM()
RATIONAL_B_SPLINE_CURVE((1.85571966561192,1.99926008128974,1.99926008128974))
REPRESENTATION_ITEM('')
);
#106=(
BOUNDED_CURVE()
B_SPLINE_CURVE(2,(#9311,#9312,#9313),.UNSPECIFIED.,.F.,.F.)
B_SPLINE_CURVE_WITH_KNOTS((3,3),(-2.73681737299457,-1.98462831214807),
 .UNSPECIFIED.)
CURVE()
GEOMETRIC_REPRESENTATION_ITEM()
RATIONAL_B_SPLINE_CURVE((1.85571966561192,1.99926008128974,1.99926008128974))
REPRESENTATION_ITEM('')
);
#107=(
BOUNDED_CURVE()
B_SPLINE_CURVE(2,(#9314,#9315,#9316),.UNSPECIFIED.,.F.,.F.)
B_SPLINE_CURVE_WITH_KNOTS((3,3),(-1.98462831214807,-1.23243925130157),
 .UNSPECIFIED.)
CURVE()
GEOMETRIC_REPRESENTATION_ITEM()
RATIONAL_B_SPLINE_CURVE((1.99926008128974,1.99926008128974,1.85571966561192))
REPRESENTATION_ITEM('')
);
#108=(
BOUNDED_CURVE()
B_SPLINE_CURVE(2,(#9318,#9319,#9320),.UNSPECIFIED.,.F.,.F.)
B_SPLINE_CURVE_WITH_KNOTS((3,3),(1.98462831214807,2.73681737299457),
 .UNSPECIFIED.)
CURVE()
GEOMETRIC_REPRESENTATION_ITEM()
RATIONAL_B_SPLINE_CURVE((1.99926008128974,1.99926008128974,1.85571966561192))
REPRESENTATION_ITEM('')
);
#109=(
BOUNDED_CURVE()
B_SPLINE_CURVE(2,(#9321,#9322,#9323),.UNSPECIFIED.,.F.,.F.)
B_SPLINE_CURVE_WITH_KNOTS((3,3),(1.23243925130157,1.98462831214807),
 .UNSPECIFIED.)
CURVE()
GEOMETRIC_REPRESENTATION_ITEM()
RATIONAL_B_SPLINE_CURVE((1.85571966561192,1.99926008128974,1.99926008128974))
REPRESENTATION_ITEM('')
);
#110=(
BOUNDED_CURVE()
B_SPLINE_CURVE(2,(#9326,#9327,#9328),.UNSPECIFIED.,.F.,.F.)
B_SPLINE_CURVE_WITH_KNOTS((3,3),(-2.73681737299457,-1.98462831214806),
 .UNSPECIFIED.)
CURVE()
GEOMETRIC_REPRESENTATION_ITEM()
RATIONAL_B_SPLINE_CURVE((1.85571966561192,1.99926008128974,1.99926008128974))
REPRESENTATION_ITEM('')
);
#111=(
BOUNDED_CURVE()
B_SPLINE_CURVE(2,(#9329,#9330,#9331),.UNSPECIFIED.,.F.,.F.)
B_SPLINE_CURVE_WITH_KNOTS((3,3),(-1.98462831214806,-1.23243925130156),
 .UNSPECIFIED.)
CURVE()
GEOMETRIC_REPRESENTATION_ITEM()
RATIONAL_B_SPLINE_CURVE((1.99926008128974,1.99926008128974,1.85571966561192))
REPRESENTATION_ITEM('')
);
#112=(
BOUNDED_CURVE()
B_SPLINE_CURVE(2,(#9333,#9334,#9335),.UNSPECIFIED.,.F.,.F.)
B_SPLINE_CURVE_WITH_KNOTS((3,3),(1.98462831214807,2.73681737299457),
 .UNSPECIFIED.)
CURVE()
GEOMETRIC_REPRESENTATION_ITEM()
RATIONAL_B_SPLINE_CURVE((1.99926008128974,1.99926008128974,1.85571966561191))
REPRESENTATION_ITEM('')
);
#113=(
BOUNDED_CURVE()
B_SPLINE_CURVE(2,(#9336,#9337,#9338),.UNSPECIFIED.,.F.,.F.)
B_SPLINE_CURVE_WITH_KNOTS((3,3),(1.23243925130156,1.98462831214807),
 .UNSPECIFIED.)
CURVE()
GEOMETRIC_REPRESENTATION_ITEM()
RATIONAL_B_SPLINE_CURVE((1.85571966561192,1.99926008128974,1.99926008128974))
REPRESENTATION_ITEM('')
);
#131=CONICAL_SURFACE('',#6019,6.5,1.0471975511966);
#132=CONICAL_SURFACE('',#6021,6.5,1.0471975511966);
#133=CONICAL_SURFACE('',#6029,6.5,1.0471975511966);
#134=CONICAL_SURFACE('',#6031,6.5,1.0471975511966);
#135=CONICAL_SURFACE('',#6033,6.5,1.0471975511966);
#136=CONICAL_SURFACE('',#6035,6.5,1.0471975511966);
#137=CONICAL_SURFACE('',#6037,6.5,1.0471975511966);
#138=CONICAL_SURFACE('',#6040,6.5,1.0471975511966);
#139=CONICAL_SURFACE('',#6042,6.5,1.0471975511966);
#140=CONICAL_SURFACE('',#6044,6.5,1.0471975511966);
#141=CONICAL_SURFACE('',#6046,6.5,1.0471975511966);
#142=CONICAL_SURFACE('',#6048,6.5,1.0471975511966);
#151=SHAPE_REPRESENTATION_RELATIONSHIP('SRR','None',#10456,#159);
#159=ADVANCED_BREP_SHAPE_REPRESENTATION('',(#175),#10408);
#167=STYLED_ITEM('',(#10503),#175);
#175=MANIFOLD_SOLID_BREP('Body1',#5302);
#201=FACE_BOUND('',#822,.T.);
#202=FACE_BOUND('',#829,.T.);
#245=PLANE('',#6023);
#246=PLANE('',#6024);
#247=PLANE('',#6025);
#248=PLANE('',#6026);
#249=PLANE('',#6027);
#250=PLANE('',#6028);
#251=PLANE('',#6039);
#252=PLANE('',#6050);
#496=FACE_OUTER_BOUND('',#807,.T.);
#497=FACE_OUTER_BOUND('',#808,.T.);
#498=FACE_OUTER_BOUND('',#809,.T.);
#499=FACE_OUTER_BOUND('',#810,.T.);
#500=FACE_OUTER_BOUND('',#811,.T.);
#501=FACE_OUTER_BOUND('',#812,.T.);
#502=FACE_OUTER_BOUND('',#813,.T.);
#503=FACE_OUTER_BOUND('',#814,.T.);
#504=FACE_OUTER_BOUND('',#815,.T.);
#505=FACE_OUTER_BOUND('',#816,.T.);
#506=FACE_OUTER_BOUND('',#817,.T.);
#507=FACE_OUTER_BOUND('',#818,.T.);
#508=FACE_OUTER_BOUND('',#819,.T.);
#509=FACE_OUTER_BOUND('',#820,.T.);
#510=FACE_OUTER_BOUND('',#821,.T.);
#511=FACE_OUTER_BOUND('',#823,.T.);
#512=FACE_OUTER_BOUND('',#824,.T.);
#513=FACE_OUTER_BOUND('',#825,.T.);
#514=FACE_OUTER_BOUND('',#826,.T.);
#515=FACE_OUTER_BOUND('',#827,.T.);
#516=FACE_OUTER_BOUND('',#828,.T.);
#807=EDGE_LOOP('',(#4478,#4479,#4480,#4481));
#808=EDGE_LOOP('',(#4482,#4483,#4484));
#809=EDGE_LOOP('',(#4485,#4486,#4487));
#810=EDGE_LOOP('',(#4488,#4489,#4490,#4491,#4492,#4493));
#811=EDGE_LOOP('',(#4494,#4495,#4496,#4497,#4498,#4499));
#812=EDGE_LOOP('',(#4500,#4501,#4502,#4503,#4504,#4505));
#813=EDGE_LOOP('',(#4506,#4507,#4508,#4509,#4510,#4511));
#814=EDGE_LOOP('',(#4512,#4513,#4514,#4515,#4516,#4517));
#815=EDGE_LOOP('',(#4518,#4519,#4520,#4521,#4522,#4523));
#816=EDGE_LOOP('',(#4524,#4525,#4526));
#817=EDGE_LOOP('',(#4527,#4528,#4529));
#818=EDGE_LOOP('',(#4530,#4531,#4532));
#819=EDGE_LOOP('',(#4533,#4534,#4535));
#820=EDGE_LOOP('',(#4536,#4537,#4538));
#821=EDGE_LOOP('',(#4539,#4540,#4541,#4542,#4543,#4544));
#822=EDGE_LOOP('',(#4545));
#823=EDGE_LOOP('',(#4546,#4547,#4548));
#824=EDGE_LOOP('',(#4549,#4550,#4551));
#825=EDGE_LOOP('',(#4552,#4553,#4554));
#826=EDGE_LOOP('',(#4555,#4556,#4557));
#827=EDGE_LOOP('',(#4558,#4559,#4560));
#828=EDGE_LOOP('',(#4561,#4562,#4563,#4564,#4565,#4566));
#829=EDGE_LOOP('',(#4567));
#1128=LINE('',#9225,#1419);
#1129=LINE('',#9250,#1420);
#1130=LINE('',#9256,#1421);
#1131=LINE('',#9263,#1422);
#1132=LINE('',#9273,#1423);
#1133=LINE('',#9291,#1424);
#1134=LINE('',#9309,#1425);
#1419=VECTOR('',#7628,3.4);
#1420=VECTOR('',#7641,1000.);
#1421=VECTOR('',#7642,1000.);
#1422=VECTOR('',#7645,1000.);
#1423=VECTOR('',#7648,1000.);
#1424=VECTOR('',#7651,1000.);
#1425=VECTOR('',#7654,1000.);
#1870=CIRCLE('',#6017,3.4);
#1871=CIRCLE('',#6018,3.4);
#1872=CIRCLE('',#6020,6.5);
#1873=CIRCLE('',#6022,6.5);
#1874=CIRCLE('',#6030,6.5);
#1875=CIRCLE('',#6032,6.5);
#1876=CIRCLE('',#6034,6.5);
#1877=CIRCLE('',#6036,6.5);
#1878=CIRCLE('',#6038,6.5);
#1879=CIRCLE('',#6041,6.5);
#1880=CIRCLE('',#6043,6.5);
#1881=CIRCLE('',#6045,6.5);
#1882=CIRCLE('',#6047,6.5);
#1883=CIRCLE('',#6049,6.5);
#2335=VERTEX_POINT('',#9222);
#2336=VERTEX_POINT('',#9224);
#2337=VERTEX_POINT('',#9228);
#2338=VERTEX_POINT('',#9229);
#2339=VERTEX_POINT('',#9231);
#2340=VERTEX_POINT('',#9239);
#2341=VERTEX_POINT('',#9240);
#2342=VERTEX_POINT('',#9242);
#2343=VERTEX_POINT('',#9251);
#2344=VERTEX_POINT('',#9255);
#2345=VERTEX_POINT('',#9261);
#2346=VERTEX_POINT('',#9262);
#2347=VERTEX_POINT('',#9271);
#2348=VERTEX_POINT('',#9272);
#2349=VERTEX_POINT('',#9274);
#2350=VERTEX_POINT('',#9281);
#2351=VERTEX_POINT('',#9289);
#2352=VERTEX_POINT('',#9290);
#2353=VERTEX_POINT('',#9292);
#2354=VERTEX_POINT('',#9299);
#2355=VERTEX_POINT('',#9307);
#2356=VERTEX_POINT('',#9308);
#2357=VERTEX_POINT('',#9310);
#2358=VERTEX_POINT('',#9317);
#2359=VERTEX_POINT('',#9325);
#2360=VERTEX_POINT('',#9332);
#3064=EDGE_CURVE('',#2335,#2335,#1870,.T.);
#3065=EDGE_CURVE('',#2335,#2336,#1128,.T.);
#3066=EDGE_CURVE('',#2336,#2336,#1871,.T.);
#3067=EDGE_CURVE('',#2337,#2338,#1872,.T.);
#3068=EDGE_CURVE('',#2339,#2338,#90,.T.);
#3069=EDGE_CURVE('',#2337,#2339,#91,.T.);
#3070=EDGE_CURVE('',#2340,#2341,#1873,.T.);
#3071=EDGE_CURVE('',#2341,#2342,#92,.T.);
#3072=EDGE_CURVE('',#2342,#2340,#93,.T.);
#3073=EDGE_CURVE('',#2339,#2342,#1129,.T.);
#3074=EDGE_CURVE('',#2338,#2343,#94,.T.);
#3075=EDGE_CURVE('',#2343,#2344,#1130,.T.);
#3076=EDGE_CURVE('',#2340,#2344,#95,.T.);
#3077=EDGE_CURVE('',#2345,#2346,#1131,.T.);
#3078=EDGE_CURVE('',#2345,#2337,#96,.T.);
#3079=EDGE_CURVE('',#2346,#2341,#97,.T.);
#3080=EDGE_CURVE('',#2347,#2348,#1132,.T.);
#3081=EDGE_CURVE('',#2347,#2349,#98,.T.);
#3082=EDGE_CURVE('',#2349,#2345,#99,.T.);
#3083=EDGE_CURVE('',#2350,#2346,#100,.T.);
#3084=EDGE_CURVE('',#2348,#2350,#101,.T.);
#3085=EDGE_CURVE('',#2351,#2352,#1133,.T.);
#3086=EDGE_CURVE('',#2351,#2353,#102,.T.);
#3087=EDGE_CURVE('',#2353,#2347,#103,.T.);
#3088=EDGE_CURVE('',#2354,#2348,#104,.T.);
#3089=EDGE_CURVE('',#2352,#2354,#105,.T.);
#3090=EDGE_CURVE('',#2355,#2356,#1134,.T.);
#3091=EDGE_CURVE('',#2355,#2357,#106,.T.);
#3092=EDGE_CURVE('',#2357,#2351,#107,.T.);
#3093=EDGE_CURVE('',#2358,#2352,#108,.T.);
#3094=EDGE_CURVE('',#2356,#2358,#109,.T.);
#3095=EDGE_CURVE('',#2343,#2359,#110,.T.);
#3096=EDGE_CURVE('',#2359,#2355,#111,.T.);
#3097=EDGE_CURVE('',#2360,#2356,#112,.T.);
#3098=EDGE_CURVE('',#2344,#2360,#113,.T.);
#3099=EDGE_CURVE('',#2354,#2358,#1874,.T.);
#3100=EDGE_CURVE('',#2350,#2354,#1875,.T.);
#3101=EDGE_CURVE('',#2341,#2350,#1876,.T.);
#3102=EDGE_CURVE('',#2340,#2360,#1877,.T.);
#3103=EDGE_CURVE('',#2358,#2360,#1878,.T.);
#3104=EDGE_CURVE('',#2357,#2353,#1879,.T.);
#3105=EDGE_CURVE('',#2359,#2357,#1880,.T.);
#3106=EDGE_CURVE('',#2338,#2359,#1881,.T.);
#3107=EDGE_CURVE('',#2349,#2337,#1882,.T.);
#3108=EDGE_CURVE('',#2353,#2349,#1883,.T.);
#4478=ORIENTED_EDGE('',*,*,#3064,.F.);
#4479=ORIENTED_EDGE('',*,*,#3065,.T.);
#4480=ORIENTED_EDGE('',*,*,#3066,.T.);
#4481=ORIENTED_EDGE('',*,*,#3065,.F.);
#4482=ORIENTED_EDGE('',*,*,#3067,.T.);
#4483=ORIENTED_EDGE('',*,*,#3068,.F.);
#4484=ORIENTED_EDGE('',*,*,#3069,.F.);
#4485=ORIENTED_EDGE('',*,*,#3070,.T.);
#4486=ORIENTED_EDGE('',*,*,#3071,.T.);
#4487=ORIENTED_EDGE('',*,*,#3072,.T.);
#4488=ORIENTED_EDGE('',*,*,#3073,.F.);
#4489=ORIENTED_EDGE('',*,*,#3068,.T.);
#4490=ORIENTED_EDGE('',*,*,#3074,.T.);
#4491=ORIENTED_EDGE('',*,*,#3075,.T.);
#4492=ORIENTED_EDGE('',*,*,#3076,.F.);
#4493=ORIENTED_EDGE('',*,*,#3072,.F.);
#4494=ORIENTED_EDGE('',*,*,#3077,.F.);
#4495=ORIENTED_EDGE('',*,*,#3078,.T.);
#4496=ORIENTED_EDGE('',*,*,#3069,.T.);
#4497=ORIENTED_EDGE('',*,*,#3073,.T.);
#4498=ORIENTED_EDGE('',*,*,#3071,.F.);
#4499=ORIENTED_EDGE('',*,*,#3079,.F.);
#4500=ORIENTED_EDGE('',*,*,#3080,.F.);
#4501=ORIENTED_EDGE('',*,*,#3081,.T.);
#4502=ORIENTED_EDGE('',*,*,#3082,.T.);
#4503=ORIENTED_EDGE('',*,*,#3077,.T.);
#4504=ORIENTED_EDGE('',*,*,#3083,.F.);
#4505=ORIENTED_EDGE('',*,*,#3084,.F.);
#4506=ORIENTED_EDGE('',*,*,#3085,.F.);
#4507=ORIENTED_EDGE('',*,*,#3086,.T.);
#4508=ORIENTED_EDGE('',*,*,#3087,.T.);
#4509=ORIENTED_EDGE('',*,*,#3080,.T.);
#4510=ORIENTED_EDGE('',*,*,#3088,.F.);
#4511=ORIENTED_EDGE('',*,*,#3089,.F.);
#4512=ORIENTED_EDGE('',*,*,#3090,.F.);
#4513=ORIENTED_EDGE('',*,*,#3091,.T.);
#4514=ORIENTED_EDGE('',*,*,#3092,.T.);
#4515=ORIENTED_EDGE('',*,*,#3085,.T.);
#4516=ORIENTED_EDGE('',*,*,#3093,.F.);
#4517=ORIENTED_EDGE('',*,*,#3094,.F.);
#4518=ORIENTED_EDGE('',*,*,#3075,.F.);
#4519=ORIENTED_EDGE('',*,*,#3095,.T.);
#4520=ORIENTED_EDGE('',*,*,#3096,.T.);
#4521=ORIENTED_EDGE('',*,*,#3090,.T.);
#4522=ORIENTED_EDGE('',*,*,#3097,.F.);
#4523=ORIENTED_EDGE('',*,*,#3098,.F.);
#4524=ORIENTED_EDGE('',*,*,#3089,.T.);
#4525=ORIENTED_EDGE('',*,*,#3099,.T.);
#4526=ORIENTED_EDGE('',*,*,#3093,.T.);
#4527=ORIENTED_EDGE('',*,*,#3084,.T.);
#4528=ORIENTED_EDGE('',*,*,#3100,.T.);
#4529=ORIENTED_EDGE('',*,*,#3088,.T.);
#4530=ORIENTED_EDGE('',*,*,#3083,.T.);
#4531=ORIENTED_EDGE('',*,*,#3079,.T.);
#4532=ORIENTED_EDGE('',*,*,#3101,.T.);
#4533=ORIENTED_EDGE('',*,*,#3076,.T.);
#4534=ORIENTED_EDGE('',*,*,#3098,.T.);
#4535=ORIENTED_EDGE('',*,*,#3102,.F.);
#4536=ORIENTED_EDGE('',*,*,#3094,.T.);
#4537=ORIENTED_EDGE('',*,*,#3103,.T.);
#4538=ORIENTED_EDGE('',*,*,#3097,.T.);
#4539=ORIENTED_EDGE('',*,*,#3103,.F.);
#4540=ORIENTED_EDGE('',*,*,#3099,.F.);
#4541=ORIENTED_EDGE('',*,*,#3100,.F.);
#4542=ORIENTED_EDGE('',*,*,#3101,.F.);
#4543=ORIENTED_EDGE('',*,*,#3070,.F.);
#4544=ORIENTED_EDGE('',*,*,#3102,.T.);
#4545=ORIENTED_EDGE('',*,*,#3066,.F.);
#4546=ORIENTED_EDGE('',*,*,#3092,.F.);
#4547=ORIENTED_EDGE('',*,*,#3104,.T.);
#4548=ORIENTED_EDGE('',*,*,#3086,.F.);
#4549=ORIENTED_EDGE('',*,*,#3096,.F.);
#4550=ORIENTED_EDGE('',*,*,#3105,.T.);
#4551=ORIENTED_EDGE('',*,*,#3091,.F.);
#4552=ORIENTED_EDGE('',*,*,#3106,.T.);
#4553=ORIENTED_EDGE('',*,*,#3095,.F.);
#4554=ORIENTED_EDGE('',*,*,#3074,.F.);
#4555=ORIENTED_EDGE('',*,*,#3107,.T.);
#4556=ORIENTED_EDGE('',*,*,#3078,.F.);
#4557=ORIENTED_EDGE('',*,*,#3082,.F.);
#4558=ORIENTED_EDGE('',*,*,#3087,.F.);
#4559=ORIENTED_EDGE('',*,*,#3108,.T.);
#4560=ORIENTED_EDGE('',*,*,#3081,.F.);
#4561=ORIENTED_EDGE('',*,*,#3108,.F.);
#4562=ORIENTED_EDGE('',*,*,#3104,.F.);
#4563=ORIENTED_EDGE('',*,*,#3105,.F.);
#4564=ORIENTED_EDGE('',*,*,#3106,.F.);
#4565=ORIENTED_EDGE('',*,*,#3067,.F.);
#4566=ORIENTED_EDGE('',*,*,#3107,.F.);
#4567=ORIENTED_EDGE('',*,*,#3064,.T.);
#4989=CYLINDRICAL_SURFACE('',#6016,3.4);
#5230=ADVANCED_FACE('',(#496),#4989,.F.);
#5231=ADVANCED_FACE('',(#497),#131,.T.);
#5232=ADVANCED_FACE('',(#498),#132,.T.);
#5233=ADVANCED_FACE('',(#499),#245,.F.);
#5234=ADVANCED_FACE('',(#500),#246,.F.);
#5235=ADVANCED_FACE('',(#501),#247,.F.);
#5236=ADVANCED_FACE('',(#502),#248,.F.);
#5237=ADVANCED_FACE('',(#503),#249,.F.);
#5238=ADVANCED_FACE('',(#504),#250,.F.);
#5239=ADVANCED_FACE('',(#505),#133,.T.);
#5240=ADVANCED_FACE('',(#506),#134,.T.);
#5241=ADVANCED_FACE('',(#507),#135,.T.);
#5242=ADVANCED_FACE('',(#508),#136,.T.);
#5243=ADVANCED_FACE('',(#509),#137,.T.);
#5244=ADVANCED_FACE('',(#510,#201),#251,.F.);
#5245=ADVANCED_FACE('',(#511),#138,.T.);
#5246=ADVANCED_FACE('',(#512),#139,.T.);
#5247=ADVANCED_FACE('',(#513),#140,.T.);
#5248=ADVANCED_FACE('',(#514),#141,.T.);
#5249=ADVANCED_FACE('',(#515),#142,.T.);
#5250=ADVANCED_FACE('',(#516,#202),#252,.T.);
#5302=CLOSED_SHELL('',(#5230,#5231,#5232,#5233,#5234,#5235,#5236,#5237,
#5238,#5239,#5240,#5241,#5242,#5243,#5244,#5245,#5246,#5247,#5248,#5249,
#5250));
#6015=AXIS2_PLACEMENT_3D('',#9220,#7622,#7623);
#6016=AXIS2_PLACEMENT_3D('',#9221,#7624,#7625);
#6017=AXIS2_PLACEMENT_3D('',#9223,#7626,#7627);
#6018=AXIS2_PLACEMENT_3D('',#9226,#7629,#7630);
#6019=AXIS2_PLACEMENT_3D('',#9227,#7631,#7632);
#6020=AXIS2_PLACEMENT_3D('',#9230,#7633,#7634);
#6021=AXIS2_PLACEMENT_3D('',#9238,#7635,#7636);
#6022=AXIS2_PLACEMENT_3D('',#9241,#7637,#7638);
#6023=AXIS2_PLACEMENT_3D('',#9249,#7639,#7640);
#6024=AXIS2_PLACEMENT_3D('',#9260,#7643,#7644);
#6025=AXIS2_PLACEMENT_3D('',#9270,#7646,#7647);
#6026=AXIS2_PLACEMENT_3D('',#9288,#7649,#7650);
#6027=AXIS2_PLACEMENT_3D('',#9306,#7652,#7653);
#6028=AXIS2_PLACEMENT_3D('',#9324,#7655,#7656);
#6029=AXIS2_PLACEMENT_3D('',#9339,#7657,#7658);
#6030=AXIS2_PLACEMENT_3D('',#9340,#7659,#7660);
#6031=AXIS2_PLACEMENT_3D('',#9341,#7661,#7662);
#6032=AXIS2_PLACEMENT_3D('',#9342,#7663,#7664);
#6033=AXIS2_PLACEMENT_3D('',#9343,#7665,#7666);
#6034=AXIS2_PLACEMENT_3D('',#9344,#7667,#7668);
#6035=AXIS2_PLACEMENT_3D('',#9345,#7669,#7670);
#6036=AXIS2_PLACEMENT_3D('',#9346,#7671,#7672);
#6037=AXIS2_PLACEMENT_3D('',#9347,#7673,#7674);
#6038=AXIS2_PLACEMENT_3D('',#9348,#7675,#7676);
#6039=AXIS2_PLACEMENT_3D('',#9349,#7677,#7678);
#6040=AXIS2_PLACEMENT_3D('',#9350,#7679,#7680);
#6041=AXIS2_PLACEMENT_3D('',#9351,#7681,#7682);
#6042=AXIS2_PLACEMENT_3D('',#9352,#7683,#7684);
#6043=AXIS2_PLACEMENT_3D('',#9353,#7685,#7686);
#6044=AXIS2_PLACEMENT_3D('',#9354,#7687,#7688);
#6045=AXIS2_PLACEMENT_3D('',#9355,#7689,#7690);
#6046=AXIS2_PLACEMENT_3D('',#9356,#7691,#7692);
#6047=AXIS2_PLACEMENT_3D('',#9357,#7693,#7694);
#6048=AXIS2_PLACEMENT_3D('',#9358,#7695,#7696);
#6049=AXIS2_PLACEMENT_3D('',#9359,#7697,#7698);
#6050=AXIS2_PLACEMENT_3D('',#9360,#7699,#7700);
#7622=DIRECTION('axis',(0.,0.,1.));
#7623=DIRECTION('refdir',(1.,0.,0.));
#7624=DIRECTION('center_axis',(-1.,0.,0.));
#7625=DIRECTION('ref_axis',(0.,0.,1.));
#7626=DIRECTION('center_axis',(-1.,0.,0.));
#7627=DIRECTION('ref_axis',(0.,0.,1.));
#7628=DIRECTION('',(-1.,0.,0.));
#7629=DIRECTION('center_axis',(-1.,0.,0.));
#7630=DIRECTION('ref_axis',(0.,0.,1.));
#7631=DIRECTION('center_axis',(-1.,0.,0.));
#7632=DIRECTION('ref_axis',(0.,0.,1.));
#7633=DIRECTION('center_axis',(-1.,0.,0.));
#7634=DIRECTION('ref_axis',(0.,2.66453525910037E-15,-1.));
#7635=DIRECTION('center_axis',(1.,0.,0.));
#7636=DIRECTION('ref_axis',(0.,0.,1.));
#7637=DIRECTION('center_axis',(1.,0.,0.));
#7638=DIRECTION('ref_axis',(0.,0.,-1.));
#7639=DIRECTION('center_axis',(0.,-0.5,-0.866025403784439));
#7640=DIRECTION('ref_axis',(0.,0.866025403784439,-0.5));
#7641=DIRECTION('',(-1.,0.,0.));
#7642=DIRECTION('',(-1.,0.,0.));
#7643=DIRECTION('center_axis',(0.,0.5,-0.866025403784439));
#7644=DIRECTION('ref_axis',(0.,0.866025403784439,0.5));
#7645=DIRECTION('',(-1.,0.,0.));
#7646=DIRECTION('center_axis',(0.,1.,-4.6225064576528E-16));
#7647=DIRECTION('ref_axis',(0.,4.6225064576528E-16,1.));
#7648=DIRECTION('',(-1.,0.,0.));
#7649=DIRECTION('center_axis',(0.,0.5,0.866025403784439));
#7650=DIRECTION('ref_axis',(0.,-0.866025403784439,0.5));
#7651=DIRECTION('',(-1.,0.,0.));
#7652=DIRECTION('center_axis',(0.,-0.5,0.866025403784439));
#7653=DIRECTION('ref_axis',(0.,-0.866025403784439,-0.5));
#7654=DIRECTION('',(-1.,0.,0.));
#7655=DIRECTION('center_axis',(0.,-1.,3.4668798432396E-16));
#7656=DIRECTION('ref_axis',(0.,-3.4668798432396E-16,-1.));
#7657=DIRECTION('center_axis',(1.,0.,0.));
#7658=DIRECTION('ref_axis',(0.,-1.22464679914735E-16,-1.));
#7659=DIRECTION('center_axis',(1.,0.,0.));
#7660=DIRECTION('ref_axis',(0.,0.,-1.));
#7661=DIRECTION('center_axis',(1.,0.,0.));
#7662=DIRECTION('ref_axis',(0.,0.,1.));
#7663=DIRECTION('center_axis',(1.,0.,0.));
#7664=DIRECTION('ref_axis',(0.,0.,-1.));
#7665=DIRECTION('center_axis',(1.,0.,0.));
#7666=DIRECTION('ref_axis',(0.,0.,1.));
#7667=DIRECTION('center_axis',(1.,0.,0.));
#7668=DIRECTION('ref_axis',(0.,0.,-1.));
#7669=DIRECTION('center_axis',(1.,0.,0.));
#7670=DIRECTION('ref_axis',(0.,0.,1.));
#7671=DIRECTION('center_axis',(-1.,0.,0.));
#7672=DIRECTION('ref_axis',(0.,0.,1.));
#7673=DIRECTION('center_axis',(1.,0.,0.));
#7674=DIRECTION('ref_axis',(0.,0.,1.));
#7675=DIRECTION('center_axis',(1.,0.,0.));
#7676=DIRECTION('ref_axis',(0.,0.,-1.));
#7677=DIRECTION('center_axis',(1.,0.,0.));
#7678=DIRECTION('ref_axis',(0.,0.,-1.));
#7679=DIRECTION('center_axis',(-1.,0.,0.));
#7680=DIRECTION('ref_axis',(0.,1.89882151931499E-15,-1.));
#7681=DIRECTION('center_axis',(-1.,0.,0.));
#7682=DIRECTION('ref_axis',(0.,0.,-1.));
#7683=DIRECTION('center_axis',(-1.,0.,0.));
#7684=DIRECTION('ref_axis',(0.,0.,1.));
#7685=DIRECTION('center_axis',(-1.,0.,0.));
#7686=DIRECTION('ref_axis',(0.,0.,-1.));
#7687=DIRECTION('center_axis',(-1.,0.,0.));
#7688=DIRECTION('ref_axis',(0.,0.,1.));
#7689=DIRECTION('center_axis',(-1.,0.,0.));
#7690=DIRECTION('ref_axis',(0.,0.,1.));
#7691=DIRECTION('center_axis',(-1.,0.,0.));
#7692=DIRECTION('ref_axis',(0.,0.,1.));
#7693=DIRECTION('center_axis',(-1.,0.,0.));
#7694=DIRECTION('ref_axis',(0.,0.,-1.));
#7695=DIRECTION('center_axis',(-1.,0.,0.));
#7696=DIRECTION('ref_axis',(0.,0.,1.));
#7697=DIRECTION('center_axis',(-1.,0.,0.));
#7698=DIRECTION('ref_axis',(0.,0.,-1.));
#7699=DIRECTION('center_axis',(1.,0.,0.));
#7700=DIRECTION('ref_axis',(0.,0.,-1.));
#9220=CARTESIAN_POINT('',(0.,0.,0.));
#9221=CARTESIAN_POINT('Origin',(-3.25,0.,0.));
#9222=CARTESIAN_POINT('',(3.25,-4.163799117101E-16,-3.4));
#9223=CARTESIAN_POINT('Origin',(3.25,0.,0.));
#9224=CARTESIAN_POINT('',(-3.25,-4.163799117101E-16,-3.4));
#9225=CARTESIAN_POINT('',(-3.25,-4.163799117101E-16,-3.4));
#9226=CARTESIAN_POINT('Origin',(-3.25,0.,0.));
#9227=CARTESIAN_POINT('Origin',(3.25,0.,0.));
#9228=CARTESIAN_POINT('',(3.25,-3.25,5.62916512459885));
#9229=CARTESIAN_POINT('',(3.25,3.25,5.62916512459885));
#9230=CARTESIAN_POINT('Origin',(3.25,0.,0.));
#9231=CARTESIAN_POINT('',(2.66944341639924,1.02340605167262E-15,7.50555349946514));
#9232=CARTESIAN_POINT('Ctrl Pts',(2.66944341639009,-2.742976229949E-11,
7.50555349948097));
#9233=CARTESIAN_POINT('Ctrl Pts',(3.25,1.74166975079127,6.50000000000637));
#9234=CARTESIAN_POINT('Ctrl Pts',(3.25,3.24999999999999,5.62916512459886));
#9235=CARTESIAN_POINT('Ctrl Pts',(3.25,-3.25000000000001,5.62916512459885));
#9236=CARTESIAN_POINT('Ctrl Pts',(3.25,-1.74166975079127,6.50000000000637));
#9237=CARTESIAN_POINT('Ctrl Pts',(2.66944341639009,2.74484283507316E-11,
7.50555349948099));
#9238=CARTESIAN_POINT('Origin',(-3.25,0.,0.));
#9239=CARTESIAN_POINT('',(-3.25,3.25,5.62916512459885));
#9240=CARTESIAN_POINT('',(-3.25,-3.25,5.62916512459885));
#9241=CARTESIAN_POINT('Origin',(-3.25,0.,0.));
#9242=CARTESIAN_POINT('',(-2.66944341639924,8.87400251789783E-16,7.50555349946514));
#9243=CARTESIAN_POINT('Ctrl Pts',(-3.25,-3.25,5.62916512459885));
#9244=CARTESIAN_POINT('Ctrl Pts',(-3.25,-1.74166975079126,6.50000000000637));
#9245=CARTESIAN_POINT('Ctrl Pts',(-2.66944341639009,2.74493855841286E-11,
7.50555349948098));
#9246=CARTESIAN_POINT('Ctrl Pts',(-2.66944341639009,-2.742976229949E-11,
7.50555349948097));
#9247=CARTESIAN_POINT('Ctrl Pts',(-3.25,1.74166975079127,6.50000000000637));
#9248=CARTESIAN_POINT('Ctrl Pts',(-3.25,3.24999999999999,5.62916512459886));
#9249=CARTESIAN_POINT('Origin',(3.25,6.5,3.75277674973257));
#9250=CARTESIAN_POINT('',(3.25,8.57827996624955E-16,7.50555349946514));
#9251=CARTESIAN_POINT('',(2.66944341639923,6.5,3.75277674973257));
#9252=CARTESIAN_POINT('Ctrl Pts',(3.25,3.24999999999999,5.62916512459886));
#9253=CARTESIAN_POINT('Ctrl Pts',(3.25,4.75833024920873,4.75833024919134));
#9254=CARTESIAN_POINT('Ctrl Pts',(2.66944341639009,6.50000000002745,3.75277674971672));
#9255=CARTESIAN_POINT('',(-2.66944341639923,6.5,3.75277674973257));
#9256=CARTESIAN_POINT('',(3.25,6.5,3.75277674973257));
#9257=CARTESIAN_POINT('Ctrl Pts',(-3.25,3.25,5.62916512459885));
#9258=CARTESIAN_POINT('Ctrl Pts',(-3.25,4.75833024920873,4.75833024919133));
#9259=CARTESIAN_POINT('Ctrl Pts',(-2.66944341639009,6.50000000002744,3.75277674971672));
#9260=CARTESIAN_POINT('Origin',(3.25,8.57827996624955E-16,7.50555349946514));
#9261=CARTESIAN_POINT('',(2.66944341639924,-6.5,3.75277674973257));
#9262=CARTESIAN_POINT('',(-2.66944341639924,-6.5,3.75277674973257));
#9263=CARTESIAN_POINT('',(3.25,-6.5,3.75277674973257));
#9264=CARTESIAN_POINT('Ctrl Pts',(2.66944341639009,-6.50000000002745,3.75277674971672));
#9265=CARTESIAN_POINT('Ctrl Pts',(3.25,-4.75833024920874,4.75833024919133));
#9266=CARTESIAN_POINT('Ctrl Pts',(3.25,-3.25,5.62916512459885));
#9267=CARTESIAN_POINT('Ctrl Pts',(-2.66944341639009,-6.50000000002744,3.75277674971673));
#9268=CARTESIAN_POINT('Ctrl Pts',(-3.25,-4.75833024920873,4.75833024919134));
#9269=CARTESIAN_POINT('Ctrl Pts',(-3.25,-3.25,5.62916512459885));
#9270=CARTESIAN_POINT('Origin',(3.25,-6.5,3.75277674973257));
#9271=CARTESIAN_POINT('',(2.66944341639924,-6.5,-3.75277674973257));
#9272=CARTESIAN_POINT('',(-2.66944341639924,-6.5,-3.75277674973257));
#9273=CARTESIAN_POINT('',(3.25,-6.5,-3.75277674973257));
#9274=CARTESIAN_POINT('',(3.25,-6.5,3.00462919747432E-15));
#9275=CARTESIAN_POINT('Ctrl Pts',(2.66944341639009,-6.5,-3.75277674976425));
#9276=CARTESIAN_POINT('Ctrl Pts',(3.25,-6.5,-1.74166975081502));
#9277=CARTESIAN_POINT('Ctrl Pts',(3.25,-6.5,1.55488747964449E-14));
#9278=CARTESIAN_POINT('Ctrl Pts',(3.25,-6.5,1.55488747964449E-14));
#9279=CARTESIAN_POINT('Ctrl Pts',(3.25,-6.5,1.74166975081504));
#9280=CARTESIAN_POINT('Ctrl Pts',(2.66944341639009,-6.5,3.75277674976426));
#9281=CARTESIAN_POINT('',(-3.25,-6.5,3.00462919747432E-15));
#9282=CARTESIAN_POINT('Ctrl Pts',(-3.25,-6.5,8.88507131225421E-15));
#9283=CARTESIAN_POINT('Ctrl Pts',(-3.25,-6.5,1.74166975081504));
#9284=CARTESIAN_POINT('Ctrl Pts',(-2.66944341639009,-6.5,3.75277674976425));
#9285=CARTESIAN_POINT('Ctrl Pts',(-2.66944341639009,-6.5,-3.75277674976426));
#9286=CARTESIAN_POINT('Ctrl Pts',(-3.25,-6.5,-1.74166975081503));
#9287=CARTESIAN_POINT('Ctrl Pts',(-3.25,-6.5,8.88507131225421E-15));
#9288=CARTESIAN_POINT('Origin',(3.25,-6.5,-3.75277674973257));
#9289=CARTESIAN_POINT('',(2.66944341639924,1.85174857192461E-15,-7.50555349946513));
#9290=CARTESIAN_POINT('',(-2.66944341639924,1.85174857192461E-15,-7.50555349946513));
#9291=CARTESIAN_POINT('',(3.25,1.78461907357084E-15,-7.50555349946513));
#9292=CARTESIAN_POINT('',(3.25,-3.25,-5.62916512459885));
#9293=CARTESIAN_POINT('Ctrl Pts',(2.66944341639009,2.74386167084123E-11,
-7.50555349948098));
#9294=CARTESIAN_POINT('Ctrl Pts',(3.25,-1.74166975079127,-6.50000000000637));
#9295=CARTESIAN_POINT('Ctrl Pts',(3.25,-3.24999999999999,-5.62916512459886));
#9296=CARTESIAN_POINT('Ctrl Pts',(3.25,-3.24999999999999,-5.62916512459886));
#9297=CARTESIAN_POINT('Ctrl Pts',(3.25,-4.75833024920873,-4.75833024919134));
#9298=CARTESIAN_POINT('Ctrl Pts',(2.66944341639009,-6.50000000002745,-3.75277674971673));
#9299=CARTESIAN_POINT('',(-3.25,-3.25,-5.62916512459885));
#9300=CARTESIAN_POINT('Ctrl Pts',(-3.25,-3.25,-5.62916512459885));
#9301=CARTESIAN_POINT('Ctrl Pts',(-3.25,-4.75833024920873,-4.75833024919133));
#9302=CARTESIAN_POINT('Ctrl Pts',(-2.66944341639009,-6.50000000002744,-3.75277674971672));
#9303=CARTESIAN_POINT('Ctrl Pts',(-2.66944341639009,2.74465138839376E-11,
-7.50555349948098));
#9304=CARTESIAN_POINT('Ctrl Pts',(-3.25,-1.74166975079127,-6.50000000000637));
#9305=CARTESIAN_POINT('Ctrl Pts',(-3.25,-3.25,-5.62916512459885));
#9306=CARTESIAN_POINT('Origin',(3.25,1.78461907357084E-15,-7.50555349946513));
#9307=CARTESIAN_POINT('',(2.66944341639924,6.5,-3.75277674973257));
#9308=CARTESIAN_POINT('',(-2.66944341639924,6.5,-3.75277674973258));
#9309=CARTESIAN_POINT('',(3.25,6.5,-3.75277674973257));
#9310=CARTESIAN_POINT('',(3.25,3.25,-5.62916512459885));
#9311=CARTESIAN_POINT('Ctrl Pts',(2.66944341639009,6.50000000002744,-3.75277674971672));
#9312=CARTESIAN_POINT('Ctrl Pts',(3.25,4.75833024920874,-4.75833024919133));
#9313=CARTESIAN_POINT('Ctrl Pts',(3.25,3.25000000000001,-5.62916512459884));
#9314=CARTESIAN_POINT('Ctrl Pts',(3.25,3.25000000000001,-5.62916512459884));
#9315=CARTESIAN_POINT('Ctrl Pts',(3.25,1.74166975079128,-6.50000000000636));
#9316=CARTESIAN_POINT('Ctrl Pts',(2.66944341639009,-2.74398132501586E-11,
-7.50555349948098));
#9317=CARTESIAN_POINT('',(-3.25,3.25,-5.62916512459885));
#9318=CARTESIAN_POINT('Ctrl Pts',(-3.25,3.24999999999999,-5.62916512459886));
#9319=CARTESIAN_POINT('Ctrl Pts',(-3.25,1.74166975079126,-6.50000000000637));
#9320=CARTESIAN_POINT('Ctrl Pts',(-2.66944341639009,-2.74465138839376E-11,
-7.50555349948098));
#9321=CARTESIAN_POINT('Ctrl Pts',(-2.66944341639009,6.50000000002743,-3.75277674971672));
#9322=CARTESIAN_POINT('Ctrl Pts',(-3.25,4.75833024920872,-4.75833024919134));
#9323=CARTESIAN_POINT('Ctrl Pts',(-3.25,3.24999999999999,-5.62916512459886));
#9324=CARTESIAN_POINT('Origin',(3.25,6.5,-3.75277674973257));
#9325=CARTESIAN_POINT('',(3.25,6.5,-2.25347189810574E-15));
#9326=CARTESIAN_POINT('Ctrl Pts',(2.66944341639009,6.5,3.75277674976426));
#9327=CARTESIAN_POINT('Ctrl Pts',(3.25,6.5,1.74166975081503));
#9328=CARTESIAN_POINT('Ctrl Pts',(3.25,6.5,-7.10805704980337E-15));
#9329=CARTESIAN_POINT('Ctrl Pts',(3.25,6.5,-7.10805704980337E-15));
#9330=CARTESIAN_POINT('Ctrl Pts',(3.25,6.5,-1.74166975081504));
#9331=CARTESIAN_POINT('Ctrl Pts',(2.66944341639009,6.5,-3.75277674976425));
#9332=CARTESIAN_POINT('',(-3.25,6.5,-2.25347189810574E-15));
#9333=CARTESIAN_POINT('Ctrl Pts',(-3.25,6.5,-2.66552139367626E-15));
#9334=CARTESIAN_POINT('Ctrl Pts',(-3.25,6.5,-1.74166975081505));
#9335=CARTESIAN_POINT('Ctrl Pts',(-2.66944341639008,6.5,-3.75277674976428));
#9336=CARTESIAN_POINT('Ctrl Pts',(-2.66944341639009,6.5,3.75277674976426));
#9337=CARTESIAN_POINT('Ctrl Pts',(-3.25,6.5,1.74166975081503));
#9338=CARTESIAN_POINT('Ctrl Pts',(-3.25,6.5,-2.66552139367626E-15));
#9339=CARTESIAN_POINT('Origin',(-3.25,0.,0.));
#9340=CARTESIAN_POINT('Origin',(-3.25,0.,0.));
#9341=CARTESIAN_POINT('Origin',(-3.25,0.,0.));
#9342=CARTESIAN_POINT('Origin',(-3.25,0.,0.));
#9343=CARTESIAN_POINT('Origin',(-3.25,0.,0.));
#9344=CARTESIAN_POINT('Origin',(-3.25,0.,0.));
#9345=CARTESIAN_POINT('Origin',(-3.25,0.,0.));
#9346=CARTESIAN_POINT('Origin',(-3.25,0.,0.));
#9347=CARTESIAN_POINT('Origin',(-3.25,0.,0.));
#9348=CARTESIAN_POINT('Origin',(-3.25,0.,0.));
#9349=CARTESIAN_POINT('Origin',(-3.25,0.,0.));
#9350=CARTESIAN_POINT('Origin',(3.25,0.,0.));
#9351=CARTESIAN_POINT('Origin',(3.25,0.,0.));
#9352=CARTESIAN_POINT('Origin',(3.25,0.,0.));
#9353=CARTESIAN_POINT('Origin',(3.25,0.,0.));
#9354=CARTESIAN_POINT('Origin',(3.25,0.,0.));
#9355=CARTESIAN_POINT('Origin',(3.25,0.,0.));
#9356=CARTESIAN_POINT('Origin',(3.25,0.,0.));
#9357=CARTESIAN_POINT('Origin',(3.25,0.,0.));
#9358=CARTESIAN_POINT('Origin',(3.25,0.,0.));
#9359=CARTESIAN_POINT('Origin',(3.25,0.,0.));
#9360=CARTESIAN_POINT('Origin',(3.25,0.,0.));
#10398=UNCERTAINTY_MEASURE_WITH_UNIT(LENGTH_MEASURE(0.01),#10414,
'DISTANCE_ACCURACY_VALUE',
'Maximum model space distance between geometric entities at asserted c
onnectivities');
#10403=UNCERTAINTY_MEASURE_WITH_UNIT(LENGTH_MEASURE(0.01),#10414,
'DISTANCE_ACCURACY_VALUE',
'Maximum model space distance between geometric entities at asserted c
onnectivities');
#10408=(
GEOMETRIC_REPRESENTATION_CONTEXT(3)
GLOBAL_UNCERTAINTY_ASSIGNED_CONTEXT((#10398))
GLOBAL_UNIT_ASSIGNED_CONTEXT((#10414,#10416,#10417))
REPRESENTATION_CONTEXT('','3D')
);
#10413=(
GEOMETRIC_REPRESENTATION_CONTEXT(3)
GLOBAL_UNCERTAINTY_ASSIGNED_CONTEXT((#10403))
GLOBAL_UNIT_ASSIGNED_CONTEXT((#10414,#10416,#10417))
REPRESENTATION_CONTEXT('','3D')
);
#10414=(
LENGTH_UNIT()
NAMED_UNIT(*)
SI_UNIT(.MILLI.,.METRE.)
);
#10416=(
NAMED_UNIT(*)
PLANE_ANGLE_UNIT()
SI_UNIT($,.RADIAN.)
);
#10417=(
NAMED_UNIT(*)
SI_UNIT($,.STERADIAN.)
SOLID_ANGLE_UNIT()
);
#10422=SHAPE_DEFINITION_REPRESENTATION(#10431,#10456);
#10431=PRODUCT_DEFINITION_SHAPE('',$,#10466);
#10456=SHAPE_REPRESENTATION('',(#6015),#10408);
#10461=PRODUCT_DEFINITION_CONTEXT('part definition',#10490,'design');
#10466=PRODUCT_DEFINITION('Hex nut M8','Hex Nut M8',#10475,#10461);
#10475=PRODUCT_DEFINITION_FORMATION('',$,#10496);
#10490=APPLICATION_CONTEXT(
'Core Data for Automotive Mechanical Design Process');
#10491=PRODUCT_CONTEXT('part definition',#10490,'mechanical');
#10496=PRODUCT('Hex nut M8','Hex Nut M8',$,(#10491));
#10503=PRESENTATION_STYLE_ASSIGNMENT((#10507));
#10507=SURFACE_STYLE_USAGE(.BOTH.,#10511);
#10511=SURFACE_SIDE_STYLE('',(#10515));
#10515=SURFACE_STYLE_FILL_AREA(#10519);
#10519=FILL_AREA_STYLE('Opaque(97,158,199)',(#10523));
#10523=FILL_AREA_STYLE_COLOUR('Opaque(97,158,199)',#10527);
#10527=COLOUR_RGB('Opaque(97,158,199)',0.380392156862745,0.619607843137255,
0.780392156862745);
ENDSEC;
END-ISO-10303-21;
